ISO-10303-21;
HEADER;
/* Generated by software containing ST-Developer
 * from STEP Tools, Inc. (www.steptools.com) 
 */

FILE_DESCRIPTION(
/* description */ ('Guided pneumatic stop gate'),
/* implementation_level */ '2;1');

FILE_NAME(
/* name */ 'Clevis Pin - 6x30.step',
/* time_stamp */ '2026-10-27T21:43:45-07:00',
/* author */ (''),
/* organization */ (''),
/* preprocessor_version */ 'ST-DEVELOPER v20.2',
/* originating_system */ 'Autodesk Translation Framework v15.17.0.0',
/* authorisation */ '');

FILE_SCHEMA (('AUTOMOTIVE_DESIGN { 1 0 10303 214 3 1 1 }'));
ENDSEC;

DATA;
#10=MECHANICAL_DESIGN_GEOMETRIC_PRESENTATION_REPRESENTATION('',(#569),#14392);
#13=B_SPLINE_CURVE_WITH_KNOTS('',3,(#13893,#13894,#13895,#13896,#13897,
#13898,#13899,#13900,#13901,#13902),.UNSPECIFIED.,.F.,.F.,(4,2,2,2,4),(0.,
0.0302963256060356,0.0605926512120712,0.090883446720838,0.121174242229605),
 .UNSPECIFIED.);
#14=B_SPLINE_CURVE_WITH_KNOTS('',3,(#13905,#13906,#13907,#13908,#13909,
#13910,#13911,#13912,#13913,#13914,#13915,#13916,#13917,#13918,#13919,#13920,
#13921,#13922,#13923,#13924,#13925,#13926,#13927,#13928,#13929,#13930,#13931,
#13932,#13933,#13934,#13935,#13936,#13937,#13938),.UNSPECIFIED.,.T.,.F.,
(4,2,2,2,2,2,2,2,2,2,2,2,2,2,2,2,4),(0.,0.0302963256060358,0.0605926512120716,
0.0908834467208383,0.121174242229605,0.151465037738372,0.181755833247138,
0.212052158853174,0.24234848445921,0.272644810065246,0.302941135671282,
0.333231931180048,0.363522726688815,0.393813522197582,0.424104317706349,
0.454400643312384,0.48469696891842),.UNSPECIFIED.);
#15=B_SPLINE_CURVE_WITH_KNOTS('',3,(#13940,#13941,#13942,#13943,#13944,
#13945,#13946,#13947,#13948,#13949),.UNSPECIFIED.,.F.,.F.,(4,2,2,2,4),(0.363522726688815,
0.393813522197581,0.424104317706348,0.454400643312384,0.48469696891842),
 .UNSPECIFIED.);
#16=B_SPLINE_CURVE_WITH_KNOTS('',3,(#13950,#13951,#13952,#13953,#13954,
#13955,#13956,#13957,#13958,#13959,#13960,#13961,#13962,#13963,#13964,#13965,
#13966,#13967),.UNSPECIFIED.,.F.,.F.,(4,2,2,2,2,2,2,2,4),(0.121174242229605,
0.151465037738371,0.181755833247138,0.212052158853174,0.24234848445921,
0.272644810065246,0.302941135671281,0.333231931180048,0.363522726688815),
 .UNSPECIFIED.);
#447=CONICAL_SURFACE('',#9264,0.475,0.785398163397448);
#448=CONICAL_SURFACE('',#9272,0.255,0.785398163397449);
#485=SHAPE_REPRESENTATION_RELATIONSHIP('SRR','None',#14622,#527);
#527=ADVANCED_BREP_SHAPE_REPRESENTATION('',(#607),#14384);
#569=STYLED_ITEM('',(#14891),#607);
#607=MANIFOLD_SOLID_BREP('Body1',#7913);
#807=FACE_BOUND('',#2209,.T.);
#808=FACE_BOUND('',#2211,.T.);
#1083=PLANE('',#9262);
#1084=PLANE('',#9268);
#1085=PLANE('',#9274);
#1537=FACE_OUTER_BOUND('',#2204,.T.);
#1538=FACE_OUTER_BOUND('',#2205,.T.);
#1539=FACE_OUTER_BOUND('',#2206,.T.);
#1540=FACE_OUTER_BOUND('',#2207,.T.);
#1541=FACE_OUTER_BOUND('',#2208,.T.);
#1542=FACE_OUTER_BOUND('',#2210,.T.);
#1543=FACE_OUTER_BOUND('',#2212,.T.);
#1544=FACE_OUTER_BOUND('',#2213,.T.);
#2204=EDGE_LOOP('',(#7016,#7017,#7018,#7019,#7020,#7021));
#2205=EDGE_LOOP('',(#7022));
#2206=EDGE_LOOP('',(#7023,#7024,#7025,#7026));
#2207=EDGE_LOOP('',(#7027,#7028,#7029,#7030));
#2208=EDGE_LOOP('',(#7031));
#2209=EDGE_LOOP('',(#7032));
#2210=EDGE_LOOP('',(#7033,#7034,#7035,#7036,#7037,#7038,#7039,#7040,#7041));
#2211=EDGE_LOOP('',(#7042));
#2212=EDGE_LOOP('',(#7043,#7044,#7045,#7046));
#2213=EDGE_LOOP('',(#7047));
#2768=LINE('',#13904,#3313);
#2769=LINE('',#13974,#3314);
#2770=LINE('',#13978,#3315);
#2771=LINE('',#13985,#3316);
#2772=LINE('',#13986,#3317);
#2773=LINE('',#13990,#3318);
#3313=VECTOR('',#11627,0.08);
#3314=VECTOR('',#11636,0.475);
#3315=VECTOR('',#11641,0.5);
#3316=VECTOR('',#11650,0.3);
#3317=VECTOR('',#11651,0.3);
#3318=VECTOR('',#11656,0.255);
#3700=CIRCLE('',#9263,0.45);
#3701=CIRCLE('',#9265,0.5);
#3702=CIRCLE('',#9267,0.5);
#3703=CIRCLE('',#9269,0.3);
#3704=CIRCLE('',#9271,0.3);
#3705=CIRCLE('',#9273,0.21);
#4284=VERTEX_POINT('',#13891);
#4285=VERTEX_POINT('',#13892);
#4286=VERTEX_POINT('',#13903);
#4287=VERTEX_POINT('',#13939);
#4288=VERTEX_POINT('',#13969);
#4289=VERTEX_POINT('',#13972);
#4290=VERTEX_POINT('',#13976);
#4291=VERTEX_POINT('',#13980);
#4292=VERTEX_POINT('',#13983);
#4293=VERTEX_POINT('',#13988);
#5206=EDGE_CURVE('',#4284,#4285,#13,.T.);
#5207=EDGE_CURVE('',#4284,#4286,#2768,.T.);
#5208=EDGE_CURVE('',#4286,#4286,#14,.T.);
#5209=EDGE_CURVE('',#4287,#4284,#15,.T.);
#5210=EDGE_CURVE('',#4285,#4287,#16,.T.);
#5211=EDGE_CURVE('',#4288,#4288,#3700,.T.);
#5212=EDGE_CURVE('',#4289,#4289,#3701,.T.);
#5213=EDGE_CURVE('',#4289,#4288,#2769,.T.);
#5214=EDGE_CURVE('',#4290,#4290,#3702,.T.);
#5215=EDGE_CURVE('',#4290,#4289,#2770,.T.);
#5216=EDGE_CURVE('',#4291,#4291,#3703,.T.);
#5217=EDGE_CURVE('',#4292,#4292,#3704,.T.);
#5218=EDGE_CURVE('',#4292,#4285,#2771,.T.);
#5219=EDGE_CURVE('',#4287,#4291,#2772,.T.);
#5220=EDGE_CURVE('',#4293,#4293,#3705,.T.);
#5221=EDGE_CURVE('',#4293,#4292,#2773,.T.);
#7016=ORIENTED_EDGE('',*,*,#5206,.F.);
#7017=ORIENTED_EDGE('',*,*,#5207,.T.);
#7018=ORIENTED_EDGE('',*,*,#5208,.F.);
#7019=ORIENTED_EDGE('',*,*,#5207,.F.);
#7020=ORIENTED_EDGE('',*,*,#5209,.F.);
#7021=ORIENTED_EDGE('',*,*,#5210,.F.);
#7022=ORIENTED_EDGE('',*,*,#5211,.F.);
#7023=ORIENTED_EDGE('',*,*,#5212,.F.);
#7024=ORIENTED_EDGE('',*,*,#5213,.T.);
#7025=ORIENTED_EDGE('',*,*,#5211,.T.);
#7026=ORIENTED_EDGE('',*,*,#5213,.F.);
#7027=ORIENTED_EDGE('',*,*,#5214,.F.);
#7028=ORIENTED_EDGE('',*,*,#5215,.T.);
#7029=ORIENTED_EDGE('',*,*,#5212,.T.);
#7030=ORIENTED_EDGE('',*,*,#5215,.F.);
#7031=ORIENTED_EDGE('',*,*,#5214,.T.);
#7032=ORIENTED_EDGE('',*,*,#5216,.F.);
#7033=ORIENTED_EDGE('',*,*,#5217,.F.);
#7034=ORIENTED_EDGE('',*,*,#5218,.T.);
#7035=ORIENTED_EDGE('',*,*,#5210,.T.);
#7036=ORIENTED_EDGE('',*,*,#5219,.T.);
#7037=ORIENTED_EDGE('',*,*,#5216,.T.);
#7038=ORIENTED_EDGE('',*,*,#5219,.F.);
#7039=ORIENTED_EDGE('',*,*,#5209,.T.);
#7040=ORIENTED_EDGE('',*,*,#5206,.T.);
#7041=ORIENTED_EDGE('',*,*,#5218,.F.);
#7042=ORIENTED_EDGE('',*,*,#5208,.T.);
#7043=ORIENTED_EDGE('',*,*,#5220,.F.);
#7044=ORIENTED_EDGE('',*,*,#5221,.T.);
#7045=ORIENTED_EDGE('',*,*,#5217,.T.);
#7046=ORIENTED_EDGE('',*,*,#5221,.F.);
#7047=ORIENTED_EDGE('',*,*,#5220,.T.);
#7384=CYLINDRICAL_SURFACE('',#9261,0.08);
#7385=CYLINDRICAL_SURFACE('',#9266,0.5);
#7386=CYLINDRICAL_SURFACE('',#9270,0.3);
#7819=ADVANCED_FACE('',(#1537),#7384,.F.);
#7820=ADVANCED_FACE('',(#1538),#1083,.T.);
#7821=ADVANCED_FACE('',(#1539),#447,.T.);
#7822=ADVANCED_FACE('',(#1540),#7385,.T.);
#7823=ADVANCED_FACE('',(#1541,#807),#1084,.T.);
#7824=ADVANCED_FACE('',(#1542,#808),#7386,.T.);
#7825=ADVANCED_FACE('',(#1543),#448,.T.);
#7826=ADVANCED_FACE('',(#1544),#1085,.T.);
#7913=CLOSED_SHELL('',(#7819,#7820,#7821,#7822,#7823,#7824,#7825,#7826));
#9260=AXIS2_PLACEMENT_3D('',#13889,#11623,#11624);
#9261=AXIS2_PLACEMENT_3D('',#13890,#11625,#11626);
#9262=AXIS2_PLACEMENT_3D('',#13968,#11628,#11629);
#9263=AXIS2_PLACEMENT_3D('',#13970,#11630,#11631);
#9264=AXIS2_PLACEMENT_3D('',#13971,#11632,#11633);
#9265=AXIS2_PLACEMENT_3D('',#13973,#11634,#11635);
#9266=AXIS2_PLACEMENT_3D('',#13975,#11637,#11638);
#9267=AXIS2_PLACEMENT_3D('',#13977,#11639,#11640);
#9268=AXIS2_PLACEMENT_3D('',#13979,#11642,#11643);
#9269=AXIS2_PLACEMENT_3D('',#13981,#11644,#11645);
#9270=AXIS2_PLACEMENT_3D('',#13982,#11646,#11647);
#9271=AXIS2_PLACEMENT_3D('',#13984,#11648,#11649);
#9272=AXIS2_PLACEMENT_3D('',#13987,#11652,#11653);
#9273=AXIS2_PLACEMENT_3D('',#13989,#11654,#11655);
#9274=AXIS2_PLACEMENT_3D('',#13991,#11657,#11658);
#11623=DIRECTION('axis',(0.,0.,1.));
#11624=DIRECTION('refdir',(1.,0.,0.));
#11625=DIRECTION('center_axis',(1.,0.,0.));
#11626=DIRECTION('ref_axis',(0.,0.,-1.));
#11627=DIRECTION('',(1.,0.,0.));
#11628=DIRECTION('center_axis',(0.,1.,0.));
#11629=DIRECTION('ref_axis',(0.,0.,1.));
#11630=DIRECTION('center_axis',(0.,-1.,0.));
#11631=DIRECTION('ref_axis',(1.,0.,0.));
#11632=DIRECTION('center_axis',(0.,-1.,0.));
#11633=DIRECTION('ref_axis',(1.,0.,0.));
#11634=DIRECTION('center_axis',(0.,-1.,0.));
#11635=DIRECTION('ref_axis',(1.,0.,0.));
#11636=DIRECTION('',(0.707106781186547,0.707106781186548,8.65956056235493E-17));
#11637=DIRECTION('center_axis',(0.,-1.,0.));
#11638=DIRECTION('ref_axis',(1.,0.,0.));
#11639=DIRECTION('center_axis',(0.,-1.,0.));
#11640=DIRECTION('ref_axis',(1.,0.,0.));
#11641=DIRECTION('',(0.,1.,0.));
#11642=DIRECTION('center_axis',(0.,-1.,0.));
#11643=DIRECTION('ref_axis',(0.,0.,-1.));
#11644=DIRECTION('center_axis',(0.,-1.,0.));
#11645=DIRECTION('ref_axis',(1.,0.,0.));
#11646=DIRECTION('center_axis',(0.,-1.,0.));
#11647=DIRECTION('ref_axis',(1.,0.,0.));
#11648=DIRECTION('center_axis',(0.,-1.,0.));
#11649=DIRECTION('ref_axis',(1.,0.,0.));
#11650=DIRECTION('',(0.,1.,0.));
#11651=DIRECTION('',(0.,1.,0.));
#11652=DIRECTION('center_axis',(0.,1.,0.));
#11653=DIRECTION('ref_axis',(1.,0.,0.));
#11654=DIRECTION('center_axis',(0.,-1.,0.));
#11655=DIRECTION('ref_axis',(1.,0.,0.));
#11656=DIRECTION('',(-0.707106781186548,0.707106781186547,-8.65956056235494E-17));
#11657=DIRECTION('center_axis',(0.,-1.,0.));
#11658=DIRECTION('ref_axis',(0.,0.,-1.));
#13889=CARTESIAN_POINT('',(0.,0.,0.));
#13890=CARTESIAN_POINT('Origin',(0.,-2.7,0.));
#13891=CARTESIAN_POINT('',(-0.289136645896019,-2.7,0.08));
#13892=CARTESIAN_POINT('',(-0.3,-2.78,-2.27065106771523E-17));
#13893=CARTESIAN_POINT('Ctrl Pts',(-0.289136645896019,-2.7,0.08));
#13894=CARTESIAN_POINT('Ctrl Pts',(-0.289136645896019,-2.71009877520201,
0.08));
#13895=CARTESIAN_POINT('Ctrl Pts',(-0.289720927595908,-2.72083518625944,
0.0779717130936404));
#13896=CARTESIAN_POINT('Ctrl Pts',(-0.291799203044223,-2.74052980652726,
0.0697927537456149));
#13897=CARTESIAN_POINT('Ctrl Pts',(-0.293259762986909,-2.74949254880105,
0.0636445361887959));
#13898=CARTESIAN_POINT('Ctrl Pts',(-0.295976783522942,-2.76364324458222,
0.0494938404076284));
#13899=CARTESIAN_POINT('Ctrl Pts',(-0.297414335384467,-2.76979246713824,
0.0405305642602551));
#13900=CARTESIAN_POINT('Ctrl Pts',(-0.299439403644655,-2.77797216257078,
0.0208340363410407));
#13901=CARTESIAN_POINT('Ctrl Pts',(-0.3,-2.78,0.0100969318362556));
#13902=CARTESIAN_POINT('Ctrl Pts',(-0.3,-2.78,5.20417042793042E-18));
#13903=CARTESIAN_POINT('',(0.289136645896019,-2.7,0.08));
#13904=CARTESIAN_POINT('',(0.,-2.7,0.08));
#13905=CARTESIAN_POINT('Ctrl Pts',(0.289136645896019,-2.7,0.08));
#13906=CARTESIAN_POINT('Ctrl Pts',(0.289136645896019,-2.68990122479799,
0.08));
#13907=CARTESIAN_POINT('Ctrl Pts',(0.289720927595908,-2.67916481374056,
0.0779717130936404));
#13908=CARTESIAN_POINT('Ctrl Pts',(0.291799203044223,-2.65947019347274,
0.0697927537456147));
#13909=CARTESIAN_POINT('Ctrl Pts',(0.293259762986909,-2.65050745119895,
0.0636445361887959));
#13910=CARTESIAN_POINT('Ctrl Pts',(0.295976783522942,-2.63635675541778,
0.0494938404076283));
#13911=CARTESIAN_POINT('Ctrl Pts',(0.297414335384467,-2.63020753286176,
0.0405305642602551));
#13912=CARTESIAN_POINT('Ctrl Pts',(0.299439403644655,-2.62202783742922,
0.0208340363410406));
#13913=CARTESIAN_POINT('Ctrl Pts',(0.3,-2.62,0.0100969318362555));
#13914=CARTESIAN_POINT('Ctrl Pts',(0.3,-2.62,-0.0100969318362556));
#13915=CARTESIAN_POINT('Ctrl Pts',(0.299439403644655,-2.62202783742922,
-0.0208340363410406));
#13916=CARTESIAN_POINT('Ctrl Pts',(0.297414335384467,-2.63020753286176,
-0.0405305642602551));
#13917=CARTESIAN_POINT('Ctrl Pts',(0.295976783522942,-2.63635675541778,
-0.0494938404076283));
#13918=CARTESIAN_POINT('Ctrl Pts',(0.293259762986909,-2.65050745119895,
-0.0636445361887959));
#13919=CARTESIAN_POINT('Ctrl Pts',(0.291799203044223,-2.65947019347274,
-0.0697927537456147));
#13920=CARTESIAN_POINT('Ctrl Pts',(0.289720927595908,-2.67916481374056,
-0.0779717130936403));
#13921=CARTESIAN_POINT('Ctrl Pts',(0.289136645896019,-2.68990122479799,
-0.08));
#13922=CARTESIAN_POINT('Ctrl Pts',(0.289136645896019,-2.71009877520201,
-0.08));
#13923=CARTESIAN_POINT('Ctrl Pts',(0.289720927595908,-2.72083518625944,
-0.0779717130936404));
#13924=CARTESIAN_POINT('Ctrl Pts',(0.291799203044223,-2.74052980652726,
-0.0697927537456147));
#13925=CARTESIAN_POINT('Ctrl Pts',(0.293259762986909,-2.74949254880105,
-0.0636445361887959));
#13926=CARTESIAN_POINT('Ctrl Pts',(0.295976783522942,-2.76364324458222,
-0.0494938404076283));
#13927=CARTESIAN_POINT('Ctrl Pts',(0.297414335384467,-2.76979246713824,
-0.0405305642602551));
#13928=CARTESIAN_POINT('Ctrl Pts',(0.299439403644655,-2.77797216257078,
-0.0208340363410406));
#13929=CARTESIAN_POINT('Ctrl Pts',(0.3,-2.78,-0.0100969318362555));
#13930=CARTESIAN_POINT('Ctrl Pts',(0.3,-2.78,0.0100969318362556));
#13931=CARTESIAN_POINT('Ctrl Pts',(0.299439403644655,-2.77797216257078,
0.0208340363410407));
#13932=CARTESIAN_POINT('Ctrl Pts',(0.297414335384467,-2.76979246713824,
0.0405305642602551));
#13933=CARTESIAN_POINT('Ctrl Pts',(0.295976783522942,-2.76364324458222,
0.0494938404076284));
#13934=CARTESIAN_POINT('Ctrl Pts',(0.293259762986909,-2.74949254880105,
0.0636445361887959));
#13935=CARTESIAN_POINT('Ctrl Pts',(0.291799203044223,-2.74052980652726,
0.0697927537456149));
#13936=CARTESIAN_POINT('Ctrl Pts',(0.289720927595908,-2.72083518625944,
0.0779717130936404));
#13937=CARTESIAN_POINT('Ctrl Pts',(0.289136645896019,-2.71009877520201,
0.08));
#13938=CARTESIAN_POINT('Ctrl Pts',(0.289136645896019,-2.7,0.08));
#13939=CARTESIAN_POINT('',(-0.3,-2.62,-3.65842984849668E-17));
#13940=CARTESIAN_POINT('Ctrl Pts',(-0.3,-2.62,-3.81639164714898E-17));
#13941=CARTESIAN_POINT('Ctrl Pts',(-0.3,-2.62,0.0100969318362555));
#13942=CARTESIAN_POINT('Ctrl Pts',(-0.299439403644655,-2.62202783742922,
0.0208340363410406));
#13943=CARTESIAN_POINT('Ctrl Pts',(-0.297414335384467,-2.63020753286176,
0.040530564260255));
#13944=CARTESIAN_POINT('Ctrl Pts',(-0.295976783522942,-2.63635675541778,
0.0494938404076283));
#13945=CARTESIAN_POINT('Ctrl Pts',(-0.293259762986909,-2.65050745119895,
0.0636445361887959));
#13946=CARTESIAN_POINT('Ctrl Pts',(-0.291799203044223,-2.65947019347274,
0.0697927537456147));
#13947=CARTESIAN_POINT('Ctrl Pts',(-0.289720927595908,-2.67916481374056,
0.0779717130936404));
#13948=CARTESIAN_POINT('Ctrl Pts',(-0.289136645896019,-2.68990122479799,
0.08));
#13949=CARTESIAN_POINT('Ctrl Pts',(-0.289136645896019,-2.7,0.08));
#13950=CARTESIAN_POINT('Ctrl Pts',(-0.3,-2.78,-6.93889390390723E-18));
#13951=CARTESIAN_POINT('Ctrl Pts',(-0.3,-2.78,-0.0100969318362556));
#13952=CARTESIAN_POINT('Ctrl Pts',(-0.299439403644655,-2.77797216257078,
-0.0208340363410406));
#13953=CARTESIAN_POINT('Ctrl Pts',(-0.297414335384467,-2.76979246713824,
-0.0405305642602551));
#13954=CARTESIAN_POINT('Ctrl Pts',(-0.295976783522942,-2.76364324458222,
-0.0494938404076283));
#13955=CARTESIAN_POINT('Ctrl Pts',(-0.293259762986909,-2.74949254880105,
-0.0636445361887959));
#13956=CARTESIAN_POINT('Ctrl Pts',(-0.291799203044223,-2.74052980652726,
-0.0697927537456147));
#13957=CARTESIAN_POINT('Ctrl Pts',(-0.289720927595908,-2.72083518625944,
-0.0779717130936403));
#13958=CARTESIAN_POINT('Ctrl Pts',(-0.289136645896019,-2.71009877520201,
-0.08));
#13959=CARTESIAN_POINT('Ctrl Pts',(-0.289136645896019,-2.68990122479799,
-0.08));
#13960=CARTESIAN_POINT('Ctrl Pts',(-0.289720927595908,-2.67916481374056,
-0.0779717130936403));
#13961=CARTESIAN_POINT('Ctrl Pts',(-0.291799203044223,-2.65947019347274,
-0.0697927537456147));
#13962=CARTESIAN_POINT('Ctrl Pts',(-0.293259762986909,-2.65050745119895,
-0.0636445361887959));
#13963=CARTESIAN_POINT('Ctrl Pts',(-0.295976783522942,-2.63635675541778,
-0.0494938404076283));
#13964=CARTESIAN_POINT('Ctrl Pts',(-0.297414335384467,-2.63020753286176,
-0.0405305642602551));
#13965=CARTESIAN_POINT('Ctrl Pts',(-0.299439403644655,-2.62202783742922,
-0.0208340363410406));
#13966=CARTESIAN_POINT('Ctrl Pts',(-0.3,-2.62,-0.0100969318362556));
#13967=CARTESIAN_POINT('Ctrl Pts',(-0.3,-2.62,-1.56125112837913E-17));
#13968=CARTESIAN_POINT('Origin',(0.45,0.2,0.));
#13969=CARTESIAN_POINT('',(-0.45,0.2,-5.51091059616309E-17));
#13970=CARTESIAN_POINT('Origin',(0.,0.2,0.));
#13971=CARTESIAN_POINT('Origin',(0.,0.175,0.));
#13972=CARTESIAN_POINT('',(-0.5,0.15,-6.12323399573676E-17));
#13973=CARTESIAN_POINT('Origin',(0.,0.15,0.));
#13974=CARTESIAN_POINT('',(-0.475,0.175,-5.81707229594993E-17));
#13975=CARTESIAN_POINT('Origin',(0.,0.0750000000000002,0.));
#13976=CARTESIAN_POINT('',(-0.5,0.,-6.12323399573677E-17));
#13977=CARTESIAN_POINT('Origin',(0.,0.,0.));
#13978=CARTESIAN_POINT('',(-0.5,0.0750000000000002,-6.12323399573677E-17));
#13979=CARTESIAN_POINT('Origin',(0.3,0.,0.));
#13980=CARTESIAN_POINT('',(-0.3,0.,-3.67394039744206E-17));
#13981=CARTESIAN_POINT('Origin',(0.,0.,0.));
#13982=CARTESIAN_POINT('Origin',(0.,-1.455,0.));
#13983=CARTESIAN_POINT('',(-0.3,-2.91,-3.67394039744206E-17));
#13984=CARTESIAN_POINT('Origin',(0.,-2.91,0.));
#13985=CARTESIAN_POINT('',(-0.3,-1.455,-3.67394039744206E-17));
#13986=CARTESIAN_POINT('',(-0.3,-1.455,-3.67394039744206E-17));
#13987=CARTESIAN_POINT('Origin',(0.,-2.955,0.));
#13988=CARTESIAN_POINT('',(-0.21,-3.,-2.57175827820944E-17));
#13989=CARTESIAN_POINT('Origin',(0.,-3.,0.));
#13990=CARTESIAN_POINT('',(-0.255,-2.955,-3.12284933782575E-17));
#13991=CARTESIAN_POINT('Origin',(0.,-3.,0.));
#14336=UNCERTAINTY_MEASURE_WITH_UNIT(LENGTH_MEASURE(0.001),#14393,
'DISTANCE_ACCURACY_VALUE',
'Maximum model space distance between geometric entities at asserted c
onnectivities');
#14344=UNCERTAINTY_MEASURE_WITH_UNIT(LENGTH_MEASURE(0.001),#14393,
'DISTANCE_ACCURACY_VALUE',
'Maximum model space distance between geometric entities at asserted c
onnectivities');
#14384=(
GEOMETRIC_REPRESENTATION_CONTEXT(3)
GLOBAL_UNCERTAINTY_ASSIGNED_CONTEXT((#14336))
GLOBAL_UNIT_ASSIGNED_CONTEXT((#14393,#14395,#14396))
REPRESENTATION_CONTEXT('','3D')
);
#14392=(
GEOMETRIC_REPRESENTATION_CONTEXT(3)
GLOBAL_UNCERTAINTY_ASSIGNED_CONTEXT((#14344))
GLOBAL_UNIT_ASSIGNED_CONTEXT((#14393,#14395,#14396))
REPRESENTATION_CONTEXT('','3D')
);
#14393=(
LENGTH_UNIT()
NAMED_UNIT(*)
SI_UNIT(.CENTI.,.METRE.)
);
#14395=(
NAMED_UNIT(*)
PLANE_ANGLE_UNIT()
SI_UNIT($,.RADIAN.)
);
#14396=(
NAMED_UNIT(*)
SI_UNIT($,.STERADIAN.)
SOLID_ANGLE_UNIT()
);
#14436=SHAPE_DEFINITION_REPRESENTATION(#14555,#14622);
#14555=PRODUCT_DEFINITION_SHAPE('',$,#14670);
#14622=SHAPE_REPRESENTATION('',(#9260),#14384);
#14630=PRODUCT_DEFINITION_CONTEXT('part definition',#14773,'design');
#14670=PRODUCT_DEFINITION('Clevis Pin - 6x30','Clevis Pin - 6x30',#14717,
#14630);
#14717=PRODUCT_DEFINITION_FORMATION('',$,#14814);
#14773=APPLICATION_CONTEXT(
'Core Data for Automotive Mechanical Design Process');
#14774=PRODUCT_CONTEXT('part definition',#14773,'mechanical');
#14814=PRODUCT('Clevis Pin - 6x30','Clevis Pin - 6x30',
'Clevis Pin - 6x30',(#14774));
#14885=COLOUR_RGB('Grey',0.48,0.52,0.57);
#14886=FILL_AREA_STYLE_COLOUR('',#14885);
#14887=FILL_AREA_STYLE('',(#14886));
#14888=SURFACE_STYLE_FILL_AREA(#14887);
#14889=SURFACE_SIDE_STYLE('',(#14888));
#14890=SURFACE_STYLE_USAGE(.BOTH.,#14889);
#14891=PRESENTATION_STYLE_ASSIGNMENT((#14890));
ENDSEC;
END-ISO-10303-21;
